ISO-10303-21;
HEADER;
/* Generated by software containing ST-Developer
 * from STEP Tools, Inc. (www.steptools.com) 
 */

FILE_DESCRIPTION(
/* description */ ('Line shaft on three pillow blocks'),
/* implementation_level */ '2;1');

FILE_NAME(
/* name */ 'Socket Set Screw - M5x8.step',
/* time_stamp */ '2026-10-27T10:49:19-07:00',
/* author */ (''),
/* organization */ (''),
/* preprocessor_version */ 'ST-DEVELOPER v20.2',
/* originating_system */ 'Autodesk Translation Framework v15.17.0.0',
/* authorisation */ '');

FILE_SCHEMA (('AUTOMOTIVE_DESIGN { 1 0 10303 214 3 1 1 }'));
ENDSEC;

DATA;
#10=MECHANICAL_DESIGN_GEOMETRIC_PRESENTATION_REPRESENTATION('',(#364),#8377);
#275=CONICAL_SURFACE('',#5098,0.235,0.785398163397448);
#276=CONICAL_SURFACE('',#5102,0.2125,0.785398163397448);
#309=SHAPE_REPRESENTATION_RELATIONSHIP('SRR','None',#8526,#336);
#336=ADVANCED_BREP_SHAPE_REPRESENTATION('',(#390),#8375);
#364=STYLED_ITEM('',(#8725),#390);
#390=MANIFOLD_SOLID_BREP('Body1',#4352);
#486=FACE_BOUND('',#1232,.T.);
#634=PLANE('',#5089);
#635=PLANE('',#5090);
#636=PLANE('',#5091);
#637=PLANE('',#5092);
#638=PLANE('',#5093);
#639=PLANE('',#5094);
#640=PLANE('',#5095);
#641=PLANE('',#5096);
#642=PLANE('',#5104);
#877=FACE_OUTER_BOUND('',#1224,.T.);
#878=FACE_OUTER_BOUND('',#1225,.T.);
#879=FACE_OUTER_BOUND('',#1226,.T.);
#880=FACE_OUTER_BOUND('',#1227,.T.);
#881=FACE_OUTER_BOUND('',#1228,.T.);
#882=FACE_OUTER_BOUND('',#1229,.T.);
#883=FACE_OUTER_BOUND('',#1230,.T.);
#884=FACE_OUTER_BOUND('',#1231,.T.);
#885=FACE_OUTER_BOUND('',#1233,.T.);
#886=FACE_OUTER_BOUND('',#1234,.T.);
#887=FACE_OUTER_BOUND('',#1235,.T.);
#888=FACE_OUTER_BOUND('',#1236,.T.);
#1224=EDGE_LOOP('',(#3887,#3888,#3889,#3890));
#1225=EDGE_LOOP('',(#3891,#3892,#3893,#3894));
#1226=EDGE_LOOP('',(#3895,#3896,#3897,#3898));
#1227=EDGE_LOOP('',(#3899,#3900,#3901,#3902));
#1228=EDGE_LOOP('',(#3903,#3904,#3905,#3906));
#1229=EDGE_LOOP('',(#3907,#3908,#3909,#3910));
#1230=EDGE_LOOP('',(#3911,#3912,#3913,#3914,#3915,#3916));
#1231=EDGE_LOOP('',(#3917));
#1232=EDGE_LOOP('',(#3918,#3919,#3920,#3921,#3922,#3923));
#1233=EDGE_LOOP('',(#3924,#3925,#3926,#3927));
#1234=EDGE_LOOP('',(#3928,#3929,#3930,#3931));
#1235=EDGE_LOOP('',(#3932,#3933,#3934,#3935));
#1236=EDGE_LOOP('',(#3936));
#1537=LINE('',#8177,#1864);
#1538=LINE('',#8179,#1865);
#1539=LINE('',#8181,#1866);
#1540=LINE('',#8182,#1867);
#1541=LINE('',#8185,#1868);
#1542=LINE('',#8187,#1869);
#1543=LINE('',#8188,#1870);
#1544=LINE('',#8191,#1871);
#1545=LINE('',#8193,#1872);
#1546=LINE('',#8194,#1873);
#1547=LINE('',#8197,#1874);
#1548=LINE('',#8199,#1875);
#1549=LINE('',#8200,#1876);
#1550=LINE('',#8203,#1877);
#1551=LINE('',#8205,#1878);
#1552=LINE('',#8206,#1879);
#1553=LINE('',#8208,#1880);
#1554=LINE('',#8209,#1881);
#1555=LINE('',#8217,#1882);
#1556=LINE('',#8221,#1883);
#1557=LINE('',#8225,#1884);
#1864=VECTOR('',#6304,1.);
#1865=VECTOR('',#6305,1.);
#1866=VECTOR('',#6306,1.);
#1867=VECTOR('',#6307,1.);
#1868=VECTOR('',#6310,1.);
#1869=VECTOR('',#6311,1.);
#1870=VECTOR('',#6312,1.);
#1871=VECTOR('',#6315,1.);
#1872=VECTOR('',#6316,1.);
#1873=VECTOR('',#6317,1.);
#1874=VECTOR('',#6320,1.);
#1875=VECTOR('',#6321,1.);
#1876=VECTOR('',#6322,1.);
#1877=VECTOR('',#6325,1.);
#1878=VECTOR('',#6326,1.);
#1879=VECTOR('',#6327,1.);
#1880=VECTOR('',#6330,1.);
#1881=VECTOR('',#6331,1.);
#1882=VECTOR('',#6342,0.235);
#1883=VECTOR('',#6347,0.25);
#1884=VECTOR('',#6352,0.2125);
#2056=CIRCLE('',#5097,0.22);
#2057=CIRCLE('',#5099,0.24505);
#2058=CIRCLE('',#5101,0.24505);
#2059=CIRCLE('',#5103,0.175);
#2387=VERTEX_POINT('',#8175);
#2388=VERTEX_POINT('',#8176);
#2389=VERTEX_POINT('',#8178);
#2390=VERTEX_POINT('',#8180);
#2391=VERTEX_POINT('',#8184);
#2392=VERTEX_POINT('',#8186);
#2393=VERTEX_POINT('',#8190);
#2394=VERTEX_POINT('',#8192);
#2395=VERTEX_POINT('',#8196);
#2396=VERTEX_POINT('',#8198);
#2397=VERTEX_POINT('',#8202);
#2398=VERTEX_POINT('',#8204);
#2399=VERTEX_POINT('',#8212);
#2400=VERTEX_POINT('',#8215);
#2401=VERTEX_POINT('',#8219);
#2402=VERTEX_POINT('',#8223);
#2892=EDGE_CURVE('',#2387,#2388,#1537,.T.);
#2893=EDGE_CURVE('',#2387,#2389,#1538,.T.);
#2894=EDGE_CURVE('',#2389,#2390,#1539,.T.);
#2895=EDGE_CURVE('',#2388,#2390,#1540,.T.);
#2896=EDGE_CURVE('',#2391,#2387,#1541,.T.);
#2897=EDGE_CURVE('',#2391,#2392,#1542,.T.);
#2898=EDGE_CURVE('',#2392,#2389,#1543,.T.);
#2899=EDGE_CURVE('',#2393,#2391,#1544,.T.);
#2900=EDGE_CURVE('',#2393,#2394,#1545,.T.);
#2901=EDGE_CURVE('',#2394,#2392,#1546,.T.);
#2902=EDGE_CURVE('',#2395,#2393,#1547,.T.);
#2903=EDGE_CURVE('',#2395,#2396,#1548,.T.);
#2904=EDGE_CURVE('',#2396,#2394,#1549,.T.);
#2905=EDGE_CURVE('',#2397,#2395,#1550,.T.);
#2906=EDGE_CURVE('',#2397,#2398,#1551,.T.);
#2907=EDGE_CURVE('',#2398,#2396,#1552,.T.);
#2908=EDGE_CURVE('',#2388,#2397,#1553,.T.);
#2909=EDGE_CURVE('',#2390,#2398,#1554,.T.);
#2910=EDGE_CURVE('',#2399,#2399,#2056,.T.);
#2911=EDGE_CURVE('',#2400,#2400,#2057,.T.);
#2912=EDGE_CURVE('',#2400,#2399,#1555,.T.);
#2913=EDGE_CURVE('',#2401,#2401,#2058,.F.);
#2914=EDGE_CURVE('',#2401,#2400,#1556,.T.);
#2915=EDGE_CURVE('',#2402,#2402,#2059,.T.);
#2916=EDGE_CURVE('',#2402,#2401,#1557,.T.);
#3887=ORIENTED_EDGE('',*,*,#2892,.F.);
#3888=ORIENTED_EDGE('',*,*,#2893,.T.);
#3889=ORIENTED_EDGE('',*,*,#2894,.T.);
#3890=ORIENTED_EDGE('',*,*,#2895,.F.);
#3891=ORIENTED_EDGE('',*,*,#2896,.F.);
#3892=ORIENTED_EDGE('',*,*,#2897,.T.);
#3893=ORIENTED_EDGE('',*,*,#2898,.T.);
#3894=ORIENTED_EDGE('',*,*,#2893,.F.);
#3895=ORIENTED_EDGE('',*,*,#2899,.F.);
#3896=ORIENTED_EDGE('',*,*,#2900,.T.);
#3897=ORIENTED_EDGE('',*,*,#2901,.T.);
#3898=ORIENTED_EDGE('',*,*,#2897,.F.);
#3899=ORIENTED_EDGE('',*,*,#2902,.F.);
#3900=ORIENTED_EDGE('',*,*,#2903,.T.);
#3901=ORIENTED_EDGE('',*,*,#2904,.T.);
#3902=ORIENTED_EDGE('',*,*,#2900,.F.);
#3903=ORIENTED_EDGE('',*,*,#2905,.F.);
#3904=ORIENTED_EDGE('',*,*,#2906,.T.);
#3905=ORIENTED_EDGE('',*,*,#2907,.T.);
#3906=ORIENTED_EDGE('',*,*,#2903,.F.);
#3907=ORIENTED_EDGE('',*,*,#2908,.F.);
#3908=ORIENTED_EDGE('',*,*,#2895,.T.);
#3909=ORIENTED_EDGE('',*,*,#2909,.T.);
#3910=ORIENTED_EDGE('',*,*,#2906,.F.);
#3911=ORIENTED_EDGE('',*,*,#2909,.F.);
#3912=ORIENTED_EDGE('',*,*,#2894,.F.);
#3913=ORIENTED_EDGE('',*,*,#2898,.F.);
#3914=ORIENTED_EDGE('',*,*,#2901,.F.);
#3915=ORIENTED_EDGE('',*,*,#2904,.F.);
#3916=ORIENTED_EDGE('',*,*,#2907,.F.);
#3917=ORIENTED_EDGE('',*,*,#2910,.F.);
#3918=ORIENTED_EDGE('',*,*,#2892,.T.);
#3919=ORIENTED_EDGE('',*,*,#2908,.T.);
#3920=ORIENTED_EDGE('',*,*,#2905,.T.);
#3921=ORIENTED_EDGE('',*,*,#2902,.T.);
#3922=ORIENTED_EDGE('',*,*,#2899,.T.);
#3923=ORIENTED_EDGE('',*,*,#2896,.T.);
#3924=ORIENTED_EDGE('',*,*,#2911,.F.);
#3925=ORIENTED_EDGE('',*,*,#2912,.T.);
#3926=ORIENTED_EDGE('',*,*,#2910,.T.);
#3927=ORIENTED_EDGE('',*,*,#2912,.F.);
#3928=ORIENTED_EDGE('',*,*,#2913,.F.);
#3929=ORIENTED_EDGE('',*,*,#2914,.T.);
#3930=ORIENTED_EDGE('',*,*,#2911,.T.);
#3931=ORIENTED_EDGE('',*,*,#2914,.F.);
#3932=ORIENTED_EDGE('',*,*,#2915,.F.);
#3933=ORIENTED_EDGE('',*,*,#2916,.T.);
#3934=ORIENTED_EDGE('',*,*,#2913,.T.);
#3935=ORIENTED_EDGE('',*,*,#2916,.F.);
#3936=ORIENTED_EDGE('',*,*,#2915,.T.);
#4069=CYLINDRICAL_SURFACE('',#5100,0.24505);
#4295=ADVANCED_FACE('',(#877),#634,.F.);
#4296=ADVANCED_FACE('',(#878),#635,.F.);
#4297=ADVANCED_FACE('',(#879),#636,.F.);
#4298=ADVANCED_FACE('',(#880),#637,.F.);
#4299=ADVANCED_FACE('',(#881),#638,.F.);
#4300=ADVANCED_FACE('',(#882),#639,.F.);
#4301=ADVANCED_FACE('',(#883),#640,.F.);
#4302=ADVANCED_FACE('',(#884,#486),#641,.T.);
#4303=ADVANCED_FACE('',(#885),#275,.T.);
#4304=ADVANCED_FACE('',(#886),#4069,.T.);
#4305=ADVANCED_FACE('',(#887),#276,.T.);
#4306=ADVANCED_FACE('',(#888),#642,.T.);
#4352=CLOSED_SHELL('',(#4295,#4296,#4297,#4298,#4299,#4300,#4301,#4302,
#4303,#4304,#4305,#4306));
#5088=AXIS2_PLACEMENT_3D('',#8173,#6300,#6301);
#5089=AXIS2_PLACEMENT_3D('',#8174,#6302,#6303);
#5090=AXIS2_PLACEMENT_3D('',#8183,#6308,#6309);
#5091=AXIS2_PLACEMENT_3D('',#8189,#6313,#6314);
#5092=AXIS2_PLACEMENT_3D('',#8195,#6318,#6319);
#5093=AXIS2_PLACEMENT_3D('',#8201,#6323,#6324);
#5094=AXIS2_PLACEMENT_3D('',#8207,#6328,#6329);
#5095=AXIS2_PLACEMENT_3D('',#8210,#6332,#6333);
#5096=AXIS2_PLACEMENT_3D('',#8211,#6334,#6335);
#5097=AXIS2_PLACEMENT_3D('',#8213,#6336,#6337);
#5098=AXIS2_PLACEMENT_3D('',#8214,#6338,#6339);
#5099=AXIS2_PLACEMENT_3D('',#8216,#6340,#6341);
#5100=AXIS2_PLACEMENT_3D('',#8218,#6343,#6344);
#5101=AXIS2_PLACEMENT_3D('',#8220,#6345,#6346);
#5102=AXIS2_PLACEMENT_3D('',#8222,#6348,#6349);
#5103=AXIS2_PLACEMENT_3D('',#8224,#6350,#6351);
#5104=AXIS2_PLACEMENT_3D('',#8226,#6353,#6354);
#6300=DIRECTION('axis',(0.,0.,1.));
#6301=DIRECTION('refdir',(1.,0.,0.));
#6302=DIRECTION('center_axis',(0.866025403784439,0.,-0.5));
#6303=DIRECTION('ref_axis',(0.5,0.,0.866025403784439));
#6304=DIRECTION('',(0.5,0.,0.866025403784439));
#6305=DIRECTION('',(0.,-1.,0.));
#6306=DIRECTION('',(0.5,0.,0.866025403784439));
#6307=DIRECTION('',(0.,-1.,0.));
#6308=DIRECTION('center_axis',(1.92296268638356E-16,0.,-1.));
#6309=DIRECTION('ref_axis',(1.,0.,1.92296268638356E-16));
#6310=DIRECTION('',(1.,0.,1.92296268638356E-16));
#6311=DIRECTION('',(0.,-1.,0.));
#6312=DIRECTION('',(1.,0.,1.92296268638356E-16));
#6313=DIRECTION('center_axis',(-0.866025403784439,0.,-0.5));
#6314=DIRECTION('ref_axis',(0.5,0.,-0.866025403784439));
#6315=DIRECTION('',(0.5,0.,-0.866025403784439));
#6316=DIRECTION('',(0.,-1.,0.));
#6317=DIRECTION('',(0.5,0.,-0.866025403784438));
#6318=DIRECTION('center_axis',(-0.866025403784439,0.,0.5));
#6319=DIRECTION('ref_axis',(-0.5,0.,-0.866025403784439));
#6320=DIRECTION('',(-0.5,0.,-0.866025403784439));
#6321=DIRECTION('',(0.,-1.,0.));
#6322=DIRECTION('',(-0.5,0.,-0.866025403784439));
#6323=DIRECTION('center_axis',(-1.92296268638356E-16,0.,1.));
#6324=DIRECTION('ref_axis',(-1.,0.,-1.92296268638356E-16));
#6325=DIRECTION('',(-1.,0.,-1.92296268638356E-16));
#6326=DIRECTION('',(0.,-1.,0.));
#6327=DIRECTION('',(-1.,0.,-1.92296268638356E-16));
#6328=DIRECTION('center_axis',(0.866025403784439,0.,0.5));
#6329=DIRECTION('ref_axis',(-0.5,0.,0.866025403784439));
#6330=DIRECTION('',(-0.5,0.,0.866025403784439));
#6331=DIRECTION('',(-0.5,0.,0.866025403784439));
#6332=DIRECTION('center_axis',(0.,-1.,0.));
#6333=DIRECTION('ref_axis',(0.,0.,-1.));
#6334=DIRECTION('center_axis',(0.,1.,0.));
#6335=DIRECTION('ref_axis',(0.,0.,1.));
#6336=DIRECTION('center_axis',(0.,-1.,0.));
#6337=DIRECTION('ref_axis',(1.,0.,0.));
#6338=DIRECTION('center_axis',(0.,-1.,0.));
#6339=DIRECTION('ref_axis',(1.,0.,0.));
#6340=DIRECTION('center_axis',(0.,-1.,0.));
#6341=DIRECTION('ref_axis',(1.,0.,0.));
#6342=DIRECTION('',(0.707106781186547,0.707106781186548,8.65956056235493E-17));
#6343=DIRECTION('center_axis',(0.,-1.,0.));
#6344=DIRECTION('ref_axis',(1.,0.,0.));
#6345=DIRECTION('center_axis',(0.,1.,0.));
#6346=DIRECTION('ref_axis',(1.,0.,0.));
#6347=DIRECTION('',(0.,1.,0.));
#6348=DIRECTION('center_axis',(0.,1.,0.));
#6349=DIRECTION('ref_axis',(1.,0.,0.));
#6350=DIRECTION('center_axis',(0.,-1.,0.));
#6351=DIRECTION('ref_axis',(1.,0.,0.));
#6352=DIRECTION('',(-0.707106781186547,0.707106781186548,-8.65956056235493E-17));
#6353=DIRECTION('center_axis',(0.,-1.,0.));
#6354=DIRECTION('ref_axis',(0.,0.,-1.));
#8173=CARTESIAN_POINT('',(0.,0.,0.));
#8174=CARTESIAN_POINT('Origin',(0.0721687836487032,0.,-0.125));
#8175=CARTESIAN_POINT('',(0.0721687836487032,0.,-0.125));
#8176=CARTESIAN_POINT('',(0.144337567297406,0.,0.));
#8177=CARTESIAN_POINT('',(0.117710979560879,0.,-0.0461186027918559));
#8178=CARTESIAN_POINT('',(0.0721687836487032,-0.25,-0.125));
#8179=CARTESIAN_POINT('',(0.0721687836487032,0.,-0.125));
#8180=CARTESIAN_POINT('',(0.144337567297406,-0.25,0.));
#8181=CARTESIAN_POINT('',(0.144337567297406,-0.25,0.));
#8182=CARTESIAN_POINT('',(0.144337567297406,0.,0.));
#8183=CARTESIAN_POINT('Origin',(-0.0721687836487032,0.,-0.125));
#8184=CARTESIAN_POINT('',(-0.0721687836487032,0.,-0.125));
#8185=CARTESIAN_POINT('',(0.0739156081756484,0.,-0.125));
#8186=CARTESIAN_POINT('',(-0.0721687836487032,-0.25,-0.125));
#8187=CARTESIAN_POINT('',(-0.0721687836487032,0.,-0.125));
#8188=CARTESIAN_POINT('',(0.0721687836487032,-0.25,-0.125));
#8189=CARTESIAN_POINT('Origin',(-0.144337567297406,0.,-4.16333634234434E-17));
#8190=CARTESIAN_POINT('',(-0.144337567297406,0.,-1.76762539787485E-17));
#8191=CARTESIAN_POINT('',(-0.0987953713852306,0.,-0.0788813972081442));
#8192=CARTESIAN_POINT('',(-0.144337567297406,-0.25,-2.77555756156289E-17));
#8193=CARTESIAN_POINT('',(-0.144337567297406,0.,-1.76762539787485E-17));
#8194=CARTESIAN_POINT('',(-0.0721687836487032,-0.25,-0.125));
#8195=CARTESIAN_POINT('Origin',(-0.0721687836487033,0.,0.125));
#8196=CARTESIAN_POINT('',(-0.0721687836487033,0.,0.125));
#8197=CARTESIAN_POINT('',(-0.0627109795608791,0.,0.141381397208144));
#8198=CARTESIAN_POINT('',(-0.0721687836487033,-0.25,0.125));
#8199=CARTESIAN_POINT('',(-0.0721687836487033,0.,0.125));
#8200=CARTESIAN_POINT('',(-0.144337567297406,-0.25,-1.76762539787485E-17));
#8201=CARTESIAN_POINT('Origin',(0.0721687836487032,0.,0.125));
#8202=CARTESIAN_POINT('',(0.0721687836487032,0.,0.125));
#8203=CARTESIAN_POINT('',(0.146084391824352,0.,0.125));
#8204=CARTESIAN_POINT('',(0.0721687836487032,-0.25,0.125));
#8205=CARTESIAN_POINT('',(0.0721687836487032,0.,0.125));
#8206=CARTESIAN_POINT('',(-0.0721687836487033,-0.25,0.125));
#8207=CARTESIAN_POINT('Origin',(0.144337567297406,0.,0.));
#8208=CARTESIAN_POINT('',(0.153795371385231,0.,-0.0163813972081441));
#8209=CARTESIAN_POINT('',(0.0721687836487032,-0.25,0.125));
#8210=CARTESIAN_POINT('Origin',(0.,-0.25,0.));
#8211=CARTESIAN_POINT('Origin',(0.22,0.,0.));
#8212=CARTESIAN_POINT('',(-0.22,-8.67361737988404E-18,-2.69422295812418E-17));
#8213=CARTESIAN_POINT('Origin',(0.,0.,0.));
#8214=CARTESIAN_POINT('Origin',(0.,-0.015,0.));
#8215=CARTESIAN_POINT('',(-0.24505,-0.02505,-3.00099698131059E-17));
#8216=CARTESIAN_POINT('Origin',(0.,-0.02505,0.));
#8217=CARTESIAN_POINT('',(-0.235,-0.015,-2.87791997799628E-17));
#8218=CARTESIAN_POINT('Origin',(0.,-0.3775,0.));
#8219=CARTESIAN_POINT('',(-0.24505,-0.72995,3.00099698131059E-17));
#8220=CARTESIAN_POINT('Origin',(0.,-0.72995,0.));
#8221=CARTESIAN_POINT('',(-0.24505,-0.3775,-3.00099698131059E-17));
#8222=CARTESIAN_POINT('Origin',(0.,-0.7625,0.));
#8223=CARTESIAN_POINT('',(-0.175,-0.8,-2.14313189850787E-17));
#8224=CARTESIAN_POINT('Origin',(0.,-0.8,0.));
#8225=CARTESIAN_POINT('',(-0.2125,-0.7625,-2.60237444818813E-17));
#8226=CARTESIAN_POINT('Origin',(0.,-0.8,0.));
#8343=UNCERTAINTY_MEASURE_WITH_UNIT(LENGTH_MEASURE(0.001),#8378,
'DISTANCE_ACCURACY_VALUE',
'Maximum model space distance between geometric entities at asserted c
onnectivities');
#8345=UNCERTAINTY_MEASURE_WITH_UNIT(LENGTH_MEASURE(0.001),#8378,
'DISTANCE_ACCURACY_VALUE',
'Maximum model space distance between geometric entities at asserted c
onnectivities');
#8375=(
GEOMETRIC_REPRESENTATION_CONTEXT(3)
GLOBAL_UNCERTAINTY_ASSIGNED_CONTEXT((#8343))
GLOBAL_UNIT_ASSIGNED_CONTEXT((#8378,#8380,#8381))
REPRESENTATION_CONTEXT('','3D')
);
#8377=(
GEOMETRIC_REPRESENTATION_CONTEXT(3)
GLOBAL_UNCERTAINTY_ASSIGNED_CONTEXT((#8345))
GLOBAL_UNIT_ASSIGNED_CONTEXT((#8378,#8380,#8381))
REPRESENTATION_CONTEXT('','3D')
);
#8378=(
LENGTH_UNIT()
NAMED_UNIT(*)
SI_UNIT(.CENTI.,.METRE.)
);
#8380=(
NAMED_UNIT(*)
PLANE_ANGLE_UNIT()
SI_UNIT($,.RADIAN.)
);
#8381=(
NAMED_UNIT(*)
SI_UNIT($,.STERADIAN.)
SOLID_ANGLE_UNIT()
);
#8411=SHAPE_DEFINITION_REPRESENTATION(#8478,#8526);
#8478=PRODUCT_DEFINITION_SHAPE('',$,#8558);
#8526=SHAPE_REPRESENTATION('',(#5088),#8375);
#8528=PRODUCT_DEFINITION_CONTEXT('part definition',#8623,'design');
#8558=PRODUCT_DEFINITION('Socket Set Screw - M5x8',
'Socket Set Screw - M5x8',#8589,#8528);
#8589=PRODUCT_DEFINITION_FORMATION('',$,#8654);
#8623=APPLICATION_CONTEXT(
'Core Data for Automotive Mechanical Design Process');
#8624=PRODUCT_CONTEXT('part definition',#8623,'mechanical');
#8654=PRODUCT('Socket Set Screw - M5x8','Socket Set Screw - M5x8',
'Socket Set Screw - M5x8',(#8624));
#8719=COLOUR_RGB('Black',0.12,0.14,0.17);
#8720=FILL_AREA_STYLE_COLOUR('',#8719);
#8721=FILL_AREA_STYLE('',(#8720));
#8722=SURFACE_STYLE_FILL_AREA(#8721);
#8723=SURFACE_SIDE_STYLE('',(#8722));
#8724=SURFACE_STYLE_USAGE(.BOTH.,#8723);
#8725=PRESENTATION_STYLE_ASSIGNMENT((#8724));
ENDSEC;
END-ISO-10303-21;
